ISO-10303-21;
HEADER;
/* Generated by software containing ST-Developer
 * from STEP Tools, Inc. (www.steptools.com) 
 */

FILE_DESCRIPTION(
/* description */ ('Turntable on roller ring'),
/* implementation_level */ '2;1');

FILE_NAME(
/* name */ 'Inner race spacer (7).step',
/* time_stamp */ '2026-10-28T03:23:59-07:00',
/* author */ (''),
/* organization */ (''),
/* preprocessor_version */ 'ST-DEVELOPER v20.2',
/* originating_system */ 'Autodesk Translation Framework v15.17.0.0',
/* authorisation */ '');

FILE_SCHEMA (('AUTOMOTIVE_DESIGN { 1 0 10303 214 3 1 1 }'));
ENDSEC;

DATA;
#10=MECHANICAL_DESIGN_GEOMETRIC_PRESENTATION_REPRESENTATION('',(#660),#16281);
#541=SHAPE_REPRESENTATION_RELATIONSHIP('SRR','None',#16561,#596);
#596=ADVANCED_BREP_SHAPE_REPRESENTATION('',(#730),#16255);
#660=STYLED_ITEM('',(#16932),#730);
#730=MANIFOLD_SOLID_BREP('Body1',#8403);
#951=FACE_BOUND('',#2318,.T.);
#952=FACE_BOUND('',#2320,.T.);
#1183=PLANE('',#9829);
#1184=PLANE('',#9830);
#1616=FACE_OUTER_BOUND('',#2315,.T.);
#1617=FACE_OUTER_BOUND('',#2316,.T.);
#1618=FACE_OUTER_BOUND('',#2317,.T.);
#1619=FACE_OUTER_BOUND('',#2319,.T.);
#2315=EDGE_LOOP('',(#7169,#7170,#7171,#7172));
#2316=EDGE_LOOP('',(#7173,#7174,#7175,#7176));
#2317=EDGE_LOOP('',(#7177));
#2318=EDGE_LOOP('',(#7178));
#2319=EDGE_LOOP('',(#7179));
#2320=EDGE_LOOP('',(#7180));
#2886=LINE('',#15151,#3369);
#2887=LINE('',#15157,#3370);
#3369=VECTOR('',#12163,0.505);
#3370=VECTOR('',#12170,0.7);
#3807=CIRCLE('',#9824,0.505);
#3808=CIRCLE('',#9825,0.505);
#3809=CIRCLE('',#9827,0.7);
#3810=CIRCLE('',#9828,0.7);
#4459=VERTEX_POINT('',#15148);
#4460=VERTEX_POINT('',#15150);
#4461=VERTEX_POINT('',#15154);
#4462=VERTEX_POINT('',#15156);
#5395=EDGE_CURVE('',#4459,#4459,#3807,.T.);
#5396=EDGE_CURVE('',#4459,#4460,#2886,.T.);
#5397=EDGE_CURVE('',#4460,#4460,#3808,.T.);
#5398=EDGE_CURVE('',#4461,#4461,#3809,.T.);
#5399=EDGE_CURVE('',#4461,#4462,#2887,.T.);
#5400=EDGE_CURVE('',#4462,#4462,#3810,.T.);
#7169=ORIENTED_EDGE('',*,*,#5395,.F.);
#7170=ORIENTED_EDGE('',*,*,#5396,.T.);
#7171=ORIENTED_EDGE('',*,*,#5397,.T.);
#7172=ORIENTED_EDGE('',*,*,#5396,.F.);
#7173=ORIENTED_EDGE('',*,*,#5398,.F.);
#7174=ORIENTED_EDGE('',*,*,#5399,.T.);
#7175=ORIENTED_EDGE('',*,*,#5400,.T.);
#7176=ORIENTED_EDGE('',*,*,#5399,.F.);
#7177=ORIENTED_EDGE('',*,*,#5398,.T.);
#7178=ORIENTED_EDGE('',*,*,#5395,.T.);
#7179=ORIENTED_EDGE('',*,*,#5400,.F.);
#7180=ORIENTED_EDGE('',*,*,#5397,.F.);
#7809=CYLINDRICAL_SURFACE('',#9823,0.505);
#7810=CYLINDRICAL_SURFACE('',#9826,0.7);
#8219=ADVANCED_FACE('',(#1616),#7809,.F.);
#8220=ADVANCED_FACE('',(#1617),#7810,.T.);
#8221=ADVANCED_FACE('',(#1618,#951),#1183,.T.);
#8222=ADVANCED_FACE('',(#1619,#952),#1184,.F.);
#8403=CLOSED_SHELL('',(#8219,#8220,#8221,#8222));
#9822=AXIS2_PLACEMENT_3D('',#15146,#12157,#12158);
#9823=AXIS2_PLACEMENT_3D('',#15147,#12159,#12160);
#9824=AXIS2_PLACEMENT_3D('',#15149,#12161,#12162);
#9825=AXIS2_PLACEMENT_3D('',#15152,#12164,#12165);
#9826=AXIS2_PLACEMENT_3D('',#15153,#12166,#12167);
#9827=AXIS2_PLACEMENT_3D('',#15155,#12168,#12169);
#9828=AXIS2_PLACEMENT_3D('',#15158,#12171,#12172);
#9829=AXIS2_PLACEMENT_3D('',#15159,#12173,#12174);
#9830=AXIS2_PLACEMENT_3D('',#15160,#12175,#12176);
#12157=DIRECTION('axis',(0.,0.,1.));
#12158=DIRECTION('refdir',(1.,0.,0.));
#12159=DIRECTION('center_axis',(0.,1.,0.));
#12160=DIRECTION('ref_axis',(1.,0.,0.));
#12161=DIRECTION('center_axis',(0.,-1.,0.));
#12162=DIRECTION('ref_axis',(1.,0.,0.));
#12163=DIRECTION('',(0.,-1.,0.));
#12164=DIRECTION('center_axis',(0.,-1.,0.));
#12165=DIRECTION('ref_axis',(1.,0.,0.));
#12166=DIRECTION('center_axis',(0.,1.,0.));
#12167=DIRECTION('ref_axis',(1.,0.,0.));
#12168=DIRECTION('center_axis',(0.,1.,0.));
#12169=DIRECTION('ref_axis',(1.,0.,0.));
#12170=DIRECTION('',(0.,-1.,0.));
#12171=DIRECTION('center_axis',(0.,1.,0.));
#12172=DIRECTION('ref_axis',(1.,0.,0.));
#12173=DIRECTION('center_axis',(0.,1.,0.));
#12174=DIRECTION('ref_axis',(1.,0.,0.));
#12175=DIRECTION('center_axis',(0.,1.,0.));
#12176=DIRECTION('ref_axis',(1.,0.,0.));
#15146=CARTESIAN_POINT('',(0.,0.,0.));
#15147=CARTESIAN_POINT('Origin',(0.,15.45,3.5));
#15148=CARTESIAN_POINT('',(-0.505,15.9,3.5));
#15149=CARTESIAN_POINT('Origin',(0.,15.9,3.5));
#15150=CARTESIAN_POINT('',(-0.505,15.45,3.5));
#15151=CARTESIAN_POINT('',(-0.505,15.45,3.5));
#15152=CARTESIAN_POINT('Origin',(0.,15.45,3.5));
#15153=CARTESIAN_POINT('Origin',(0.,15.45,3.5));
#15154=CARTESIAN_POINT('',(-0.7,15.9,3.5));
#15155=CARTESIAN_POINT('Origin',(0.,15.9,3.5));
#15156=CARTESIAN_POINT('',(-0.7,15.45,3.5));
#15157=CARTESIAN_POINT('',(-0.7,15.45,3.5));
#15158=CARTESIAN_POINT('Origin',(0.,15.45,3.5));
#15159=CARTESIAN_POINT('Origin',(0.,15.9,3.5));
#15160=CARTESIAN_POINT('Origin',(0.,15.45,3.5));
#16186=UNCERTAINTY_MEASURE_WITH_UNIT(LENGTH_MEASURE(0.001),#16282,
'DISTANCE_ACCURACY_VALUE',
'Maximum model space distance between geometric entities at asserted c
onnectivities');
#16212=UNCERTAINTY_MEASURE_WITH_UNIT(LENGTH_MEASURE(0.001),#16282,
'DISTANCE_ACCURACY_VALUE',
'Maximum model space distance between geometric entities at asserted c
onnectivities');
#16255=(
GEOMETRIC_REPRESENTATION_CONTEXT(3)
GLOBAL_UNCERTAINTY_ASSIGNED_CONTEXT((#16186))
GLOBAL_UNIT_ASSIGNED_CONTEXT((#16282,#16284,#16285))
REPRESENTATION_CONTEXT('','3D')
);
#16281=(
GEOMETRIC_REPRESENTATION_CONTEXT(3)
GLOBAL_UNCERTAINTY_ASSIGNED_CONTEXT((#16212))
GLOBAL_UNIT_ASSIGNED_CONTEXT((#16282,#16284,#16285))
REPRESENTATION_CONTEXT('','3D')
);
#16282=(
LENGTH_UNIT()
NAMED_UNIT(*)
SI_UNIT(.CENTI.,.METRE.)
);
#16284=(
NAMED_UNIT(*)
PLANE_ANGLE_UNIT()
SI_UNIT($,.RADIAN.)
);
#16285=(
NAMED_UNIT(*)
SI_UNIT($,.STERADIAN.)
SOLID_ANGLE_UNIT()
);
#16328=SHAPE_DEFINITION_REPRESENTATION(#16422,#16561);
#16422=PRODUCT_DEFINITION_SHAPE('',$,#16630);
#16561=SHAPE_REPRESENTATION('',(#9822),#16255);
#16587=PRODUCT_DEFINITION_CONTEXT('part definition',#16793,'design');
#16630=PRODUCT_DEFINITION('Inner race spacer (7)','Inner race spacer (7)',
#16698,#16587);
#16698=PRODUCT_DEFINITION_FORMATION('',$,#16837);
#16793=APPLICATION_CONTEXT(
'Core Data for Automotive Mechanical Design Process');
#16794=PRODUCT_CONTEXT('part definition',#16793,'mechanical');
#16837=PRODUCT('Inner race spacer (7)','Inner race spacer (7)',
'Inner race spacer (7)',(#16794));
#16926=COLOUR_RGB('Grey',0.48,0.52,0.57);
#16927=FILL_AREA_STYLE_COLOUR('',#16926);
#16928=FILL_AREA_STYLE('',(#16927));
#16929=SURFACE_STYLE_FILL_AREA(#16928);
#16930=SURFACE_SIDE_STYLE('',(#16929));
#16931=SURFACE_STYLE_USAGE(.BOTH.,#16930);
#16932=PRESENTATION_STYLE_ASSIGNMENT((#16931));
ENDSEC;
END-ISO-10303-21;
